ISO-10303-21;
HEADER;
/* Generated by software containing ST-Developer
 * from STEP Tools, Inc. (www.steptools.com) 
 */

FILE_DESCRIPTION(
/* description */ ('Worm-less right-angle friction wheel drive'),
/* implementation_level */ '2;1');

FILE_NAME(
/* name */ 'M5x5 collar screw.step',
/* time_stamp */ '2026-10-28T03:22:36-07:00',
/* author */ (''),
/* organization */ (''),
/* preprocessor_version */ 'ST-DEVELOPER v20.2',
/* originating_system */ 'Autodesk Translation Framework v15.17.0.0',
/* authorisation */ '');

FILE_SCHEMA (('AUTOMOTIVE_DESIGN { 1 0 10303 214 3 1 1 }'));
ENDSEC;

DATA;
#10=MECHANICAL_DESIGN_GEOMETRIC_PRESENTATION_REPRESENTATION('',(#664),#17046);
#476=CONICAL_SURFACE('',#9749,0.235,0.785398163397448);
#563=SHAPE_REPRESENTATION_RELATIONSHIP('SRR','None',#17309,#610);
#610=ADVANCED_BREP_SHAPE_REPRESENTATION('',(#714),#17045);
#664=STYLED_ITEM('',(#17598),#714);
#714=MANIFOLD_SOLID_BREP('Body1',#8223);
#951=FACE_BOUND('',#2374,.T.);
#1199=PLANE('',#9738);
#1200=PLANE('',#9740);
#1201=PLANE('',#9741);
#1202=PLANE('',#9742);
#1203=PLANE('',#9743);
#1204=PLANE('',#9744);
#1205=PLANE('',#9745);
#1206=PLANE('',#9746);
#1207=PLANE('',#9747);
#1663=FACE_OUTER_BOUND('',#2365,.T.);
#1664=FACE_OUTER_BOUND('',#2366,.T.);
#1665=FACE_OUTER_BOUND('',#2367,.T.);
#1666=FACE_OUTER_BOUND('',#2368,.T.);
#1667=FACE_OUTER_BOUND('',#2369,.T.);
#1668=FACE_OUTER_BOUND('',#2370,.T.);
#1669=FACE_OUTER_BOUND('',#2371,.T.);
#1670=FACE_OUTER_BOUND('',#2372,.T.);
#1671=FACE_OUTER_BOUND('',#2373,.T.);
#1672=FACE_OUTER_BOUND('',#2375,.T.);
#1673=FACE_OUTER_BOUND('',#2376,.T.);
#2365=EDGE_LOOP('',(#7484));
#2366=EDGE_LOOP('',(#7485,#7486,#7487,#7488));
#2367=EDGE_LOOP('',(#7489,#7490,#7491,#7492));
#2368=EDGE_LOOP('',(#7493,#7494,#7495,#7496));
#2369=EDGE_LOOP('',(#7497,#7498,#7499,#7500));
#2370=EDGE_LOOP('',(#7501,#7502,#7503,#7504));
#2371=EDGE_LOOP('',(#7505,#7506,#7507,#7508));
#2372=EDGE_LOOP('',(#7509,#7510,#7511,#7512,#7513,#7514));
#2373=EDGE_LOOP('',(#7515));
#2374=EDGE_LOOP('',(#7516,#7517,#7518,#7519,#7520,#7521));
#2375=EDGE_LOOP('',(#7522,#7523,#7524,#7525));
#2376=EDGE_LOOP('',(#7526,#7527,#7528,#7529));
#2897=LINE('',#16877,#3437);
#2898=LINE('',#16879,#3438);
#2899=LINE('',#16881,#3439);
#2900=LINE('',#16882,#3440);
#2901=LINE('',#16885,#3441);
#2902=LINE('',#16887,#3442);
#2903=LINE('',#16888,#3443);
#2904=LINE('',#16891,#3444);
#2905=LINE('',#16893,#3445);
#2906=LINE('',#16894,#3446);
#2907=LINE('',#16897,#3447);
#2908=LINE('',#16899,#3448);
#2909=LINE('',#16900,#3449);
#2910=LINE('',#16903,#3450);
#2911=LINE('',#16905,#3451);
#2912=LINE('',#16906,#3452);
#2913=LINE('',#16908,#3453);
#2914=LINE('',#16909,#3454);
#2915=LINE('',#16917,#3455);
#2916=LINE('',#16919,#3456);
#3437=VECTOR('',#12291,1.);
#3438=VECTOR('',#12292,1.);
#3439=VECTOR('',#12293,1.);
#3440=VECTOR('',#12294,1.);
#3441=VECTOR('',#12297,1.);
#3442=VECTOR('',#12298,1.);
#3443=VECTOR('',#12299,1.);
#3444=VECTOR('',#12302,1.);
#3445=VECTOR('',#12303,1.);
#3446=VECTOR('',#12304,1.);
#3447=VECTOR('',#12307,1.);
#3448=VECTOR('',#12308,1.);
#3449=VECTOR('',#12309,1.);
#3450=VECTOR('',#12312,1.);
#3451=VECTOR('',#12313,1.);
#3452=VECTOR('',#12314,1.);
#3453=VECTOR('',#12317,1.);
#3454=VECTOR('',#12318,1.);
#3455=VECTOR('',#12329,0.235);
#3456=VECTOR('',#12332,0.25);
#3866=CIRCLE('',#9739,0.24505);
#3867=CIRCLE('',#9748,0.22);
#3868=CIRCLE('',#9750,0.24505);
#4521=VERTEX_POINT('',#16872);
#4522=VERTEX_POINT('',#16875);
#4523=VERTEX_POINT('',#16876);
#4524=VERTEX_POINT('',#16878);
#4525=VERTEX_POINT('',#16880);
#4526=VERTEX_POINT('',#16884);
#4527=VERTEX_POINT('',#16886);
#4528=VERTEX_POINT('',#16890);
#4529=VERTEX_POINT('',#16892);
#4530=VERTEX_POINT('',#16896);
#4531=VERTEX_POINT('',#16898);
#4532=VERTEX_POINT('',#16902);
#4533=VERTEX_POINT('',#16904);
#4534=VERTEX_POINT('',#16912);
#4535=VERTEX_POINT('',#16915);
#5511=EDGE_CURVE('',#4521,#4521,#3866,.T.);
#5512=EDGE_CURVE('',#4522,#4523,#2897,.T.);
#5513=EDGE_CURVE('',#4522,#4524,#2898,.T.);
#5514=EDGE_CURVE('',#4524,#4525,#2899,.T.);
#5515=EDGE_CURVE('',#4523,#4525,#2900,.T.);
#5516=EDGE_CURVE('',#4526,#4522,#2901,.T.);
#5517=EDGE_CURVE('',#4526,#4527,#2902,.T.);
#5518=EDGE_CURVE('',#4527,#4524,#2903,.T.);
#5519=EDGE_CURVE('',#4528,#4526,#2904,.T.);
#5520=EDGE_CURVE('',#4528,#4529,#2905,.T.);
#5521=EDGE_CURVE('',#4529,#4527,#2906,.T.);
#5522=EDGE_CURVE('',#4530,#4528,#2907,.T.);
#5523=EDGE_CURVE('',#4530,#4531,#2908,.T.);
#5524=EDGE_CURVE('',#4531,#4529,#2909,.T.);
#5525=EDGE_CURVE('',#4532,#4530,#2910,.T.);
#5526=EDGE_CURVE('',#4532,#4533,#2911,.T.);
#5527=EDGE_CURVE('',#4533,#4531,#2912,.T.);
#5528=EDGE_CURVE('',#4523,#4532,#2913,.T.);
#5529=EDGE_CURVE('',#4525,#4533,#2914,.T.);
#5530=EDGE_CURVE('',#4534,#4534,#3867,.T.);
#5531=EDGE_CURVE('',#4535,#4535,#3868,.T.);
#5532=EDGE_CURVE('',#4535,#4534,#2915,.T.);
#5533=EDGE_CURVE('',#4521,#4535,#2916,.T.);
#7484=ORIENTED_EDGE('',*,*,#5511,.F.);
#7485=ORIENTED_EDGE('',*,*,#5512,.F.);
#7486=ORIENTED_EDGE('',*,*,#5513,.T.);
#7487=ORIENTED_EDGE('',*,*,#5514,.T.);
#7488=ORIENTED_EDGE('',*,*,#5515,.F.);
#7489=ORIENTED_EDGE('',*,*,#5516,.F.);
#7490=ORIENTED_EDGE('',*,*,#5517,.T.);
#7491=ORIENTED_EDGE('',*,*,#5518,.T.);
#7492=ORIENTED_EDGE('',*,*,#5513,.F.);
#7493=ORIENTED_EDGE('',*,*,#5519,.F.);
#7494=ORIENTED_EDGE('',*,*,#5520,.T.);
#7495=ORIENTED_EDGE('',*,*,#5521,.T.);
#7496=ORIENTED_EDGE('',*,*,#5517,.F.);
#7497=ORIENTED_EDGE('',*,*,#5522,.F.);
#7498=ORIENTED_EDGE('',*,*,#5523,.T.);
#7499=ORIENTED_EDGE('',*,*,#5524,.T.);
#7500=ORIENTED_EDGE('',*,*,#5520,.F.);
#7501=ORIENTED_EDGE('',*,*,#5525,.F.);
#7502=ORIENTED_EDGE('',*,*,#5526,.T.);
#7503=ORIENTED_EDGE('',*,*,#5527,.T.);
#7504=ORIENTED_EDGE('',*,*,#5523,.F.);
#7505=ORIENTED_EDGE('',*,*,#5528,.F.);
#7506=ORIENTED_EDGE('',*,*,#5515,.T.);
#7507=ORIENTED_EDGE('',*,*,#5529,.T.);
#7508=ORIENTED_EDGE('',*,*,#5526,.F.);
#7509=ORIENTED_EDGE('',*,*,#5529,.F.);
#7510=ORIENTED_EDGE('',*,*,#5514,.F.);
#7511=ORIENTED_EDGE('',*,*,#5518,.F.);
#7512=ORIENTED_EDGE('',*,*,#5521,.F.);
#7513=ORIENTED_EDGE('',*,*,#5524,.F.);
#7514=ORIENTED_EDGE('',*,*,#5527,.F.);
#7515=ORIENTED_EDGE('',*,*,#5530,.F.);
#7516=ORIENTED_EDGE('',*,*,#5512,.T.);
#7517=ORIENTED_EDGE('',*,*,#5528,.T.);
#7518=ORIENTED_EDGE('',*,*,#5525,.T.);
#7519=ORIENTED_EDGE('',*,*,#5522,.T.);
#7520=ORIENTED_EDGE('',*,*,#5519,.T.);
#7521=ORIENTED_EDGE('',*,*,#5516,.T.);
#7522=ORIENTED_EDGE('',*,*,#5531,.F.);
#7523=ORIENTED_EDGE('',*,*,#5532,.T.);
#7524=ORIENTED_EDGE('',*,*,#5530,.T.);
#7525=ORIENTED_EDGE('',*,*,#5532,.F.);
#7526=ORIENTED_EDGE('',*,*,#5511,.T.);
#7527=ORIENTED_EDGE('',*,*,#5533,.T.);
#7528=ORIENTED_EDGE('',*,*,#5531,.T.);
#7529=ORIENTED_EDGE('',*,*,#5533,.F.);
#7699=CYLINDRICAL_SURFACE('',#9751,0.24505);
#8155=ADVANCED_FACE('',(#1663),#1199,.F.);
#8156=ADVANCED_FACE('',(#1664),#1200,.F.);
#8157=ADVANCED_FACE('',(#1665),#1201,.F.);
#8158=ADVANCED_FACE('',(#1666),#1202,.F.);
#8159=ADVANCED_FACE('',(#1667),#1203,.F.);
#8160=ADVANCED_FACE('',(#1668),#1204,.F.);
#8161=ADVANCED_FACE('',(#1669),#1205,.F.);
#8162=ADVANCED_FACE('',(#1670),#1206,.F.);
#8163=ADVANCED_FACE('',(#1671,#951),#1207,.T.);
#8164=ADVANCED_FACE('',(#1672),#476,.T.);
#8165=ADVANCED_FACE('',(#1673),#7699,.T.);
#8223=CLOSED_SHELL('',(#8155,#8156,#8157,#8158,#8159,#8160,#8161,#8162,
#8163,#8164,#8165));
#9737=AXIS2_PLACEMENT_3D('',#16870,#12283,#12284);
#9738=AXIS2_PLACEMENT_3D('',#16871,#12285,#12286);
#9739=AXIS2_PLACEMENT_3D('',#16873,#12287,#12288);
#9740=AXIS2_PLACEMENT_3D('',#16874,#12289,#12290);
#9741=AXIS2_PLACEMENT_3D('',#16883,#12295,#12296);
#9742=AXIS2_PLACEMENT_3D('',#16889,#12300,#12301);
#9743=AXIS2_PLACEMENT_3D('',#16895,#12305,#12306);
#9744=AXIS2_PLACEMENT_3D('',#16901,#12310,#12311);
#9745=AXIS2_PLACEMENT_3D('',#16907,#12315,#12316);
#9746=AXIS2_PLACEMENT_3D('',#16910,#12319,#12320);
#9747=AXIS2_PLACEMENT_3D('',#16911,#12321,#12322);
#9748=AXIS2_PLACEMENT_3D('',#16913,#12323,#12324);
#9749=AXIS2_PLACEMENT_3D('',#16914,#12325,#12326);
#9750=AXIS2_PLACEMENT_3D('',#16916,#12327,#12328);
#9751=AXIS2_PLACEMENT_3D('',#16918,#12330,#12331);
#12283=DIRECTION('axis',(0.,0.,1.));
#12284=DIRECTION('refdir',(1.,0.,0.));
#12285=DIRECTION('center_axis',(0.,1.,0.));
#12286=DIRECTION('ref_axis',(1.,0.,0.));
#12287=DIRECTION('center_axis',(0.,1.,0.));
#12288=DIRECTION('ref_axis',(1.,0.,0.));
#12289=DIRECTION('center_axis',(0.866025403784439,0.,-0.5));
#12290=DIRECTION('ref_axis',(0.5,0.,0.866025403784439));
#12291=DIRECTION('',(0.5,0.,0.866025403784439));
#12292=DIRECTION('',(0.,-1.,0.));
#12293=DIRECTION('',(0.5,0.,0.866025403784439));
#12294=DIRECTION('',(0.,-1.,0.));
#12295=DIRECTION('center_axis',(1.92296268638356E-16,0.,-1.));
#12296=DIRECTION('ref_axis',(1.,0.,1.92296268638356E-16));
#12297=DIRECTION('',(1.,0.,1.92296268638356E-16));
#12298=DIRECTION('',(0.,-1.,0.));
#12299=DIRECTION('',(1.,0.,1.92296268638356E-16));
#12300=DIRECTION('center_axis',(-0.866025403784439,0.,-0.5));
#12301=DIRECTION('ref_axis',(0.5,0.,-0.866025403784439));
#12302=DIRECTION('',(0.5,0.,-0.866025403784439));
#12303=DIRECTION('',(0.,-1.,0.));
#12304=DIRECTION('',(0.5,0.,-0.866025403784438));
#12305=DIRECTION('center_axis',(-0.866025403784439,0.,0.5));
#12306=DIRECTION('ref_axis',(-0.5,0.,-0.866025403784439));
#12307=DIRECTION('',(-0.5,0.,-0.866025403784439));
#12308=DIRECTION('',(0.,-1.,0.));
#12309=DIRECTION('',(-0.5,0.,-0.866025403784439));
#12310=DIRECTION('center_axis',(-1.92296268638356E-16,0.,1.));
#12311=DIRECTION('ref_axis',(-1.,0.,-1.92296268638356E-16));
#12312=DIRECTION('',(-1.,0.,-1.92296268638356E-16));
#12313=DIRECTION('',(0.,-1.,0.));
#12314=DIRECTION('',(-1.,0.,-1.92296268638356E-16));
#12315=DIRECTION('center_axis',(0.866025403784439,0.,0.5));
#12316=DIRECTION('ref_axis',(-0.5,0.,0.866025403784439));
#12317=DIRECTION('',(-0.5,0.,0.866025403784439));
#12318=DIRECTION('',(-0.5,0.,0.866025403784439));
#12319=DIRECTION('center_axis',(0.,-1.,0.));
#12320=DIRECTION('ref_axis',(0.,0.,-1.));
#12321=DIRECTION('center_axis',(0.,1.,0.));
#12322=DIRECTION('ref_axis',(0.,0.,1.));
#12323=DIRECTION('center_axis',(0.,-1.,0.));
#12324=DIRECTION('ref_axis',(1.,0.,0.));
#12325=DIRECTION('center_axis',(0.,-1.,0.));
#12326=DIRECTION('ref_axis',(1.,0.,0.));
#12327=DIRECTION('center_axis',(0.,-1.,0.));
#12328=DIRECTION('ref_axis',(1.,0.,0.));
#12329=DIRECTION('',(0.707106781186547,0.707106781186548,8.65956056235493E-17));
#12330=DIRECTION('center_axis',(0.,-1.,0.));
#12331=DIRECTION('ref_axis',(1.,0.,0.));
#12332=DIRECTION('',(0.,1.,0.));
#16870=CARTESIAN_POINT('',(0.,0.,0.));
#16871=CARTESIAN_POINT('Origin',(0.,-0.5,0.));
#16872=CARTESIAN_POINT('',(-0.24505,-0.5,3.00099698131059E-17));
#16873=CARTESIAN_POINT('Origin',(0.,-0.5,0.));
#16874=CARTESIAN_POINT('Origin',(0.0721687836487032,0.,-0.125));
#16875=CARTESIAN_POINT('',(0.0721687836487032,0.,-0.125));
#16876=CARTESIAN_POINT('',(0.144337567297406,0.,0.));
#16877=CARTESIAN_POINT('',(0.117710979560879,0.,-0.0461186027918559));
#16878=CARTESIAN_POINT('',(0.0721687836487032,-0.25,-0.125));
#16879=CARTESIAN_POINT('',(0.0721687836487032,0.,-0.125));
#16880=CARTESIAN_POINT('',(0.144337567297406,-0.25,0.));
#16881=CARTESIAN_POINT('',(0.144337567297406,-0.25,0.));
#16882=CARTESIAN_POINT('',(0.144337567297406,0.,0.));
#16883=CARTESIAN_POINT('Origin',(-0.0721687836487032,0.,-0.125));
#16884=CARTESIAN_POINT('',(-0.0721687836487032,0.,-0.125));
#16885=CARTESIAN_POINT('',(0.0739156081756484,0.,-0.125));
#16886=CARTESIAN_POINT('',(-0.0721687836487032,-0.25,-0.125));
#16887=CARTESIAN_POINT('',(-0.0721687836487032,0.,-0.125));
#16888=CARTESIAN_POINT('',(0.0721687836487032,-0.25,-0.125));
#16889=CARTESIAN_POINT('Origin',(-0.144337567297406,0.,-4.16333634234434E-17));
#16890=CARTESIAN_POINT('',(-0.144337567297406,0.,-1.76762539787485E-17));
#16891=CARTESIAN_POINT('',(-0.0987953713852306,0.,-0.0788813972081442));
#16892=CARTESIAN_POINT('',(-0.144337567297406,-0.25,-2.77555756156289E-17));
#16893=CARTESIAN_POINT('',(-0.144337567297406,0.,-1.76762539787485E-17));
#16894=CARTESIAN_POINT('',(-0.0721687836487032,-0.25,-0.125));
#16895=CARTESIAN_POINT('Origin',(-0.0721687836487033,0.,0.125));
#16896=CARTESIAN_POINT('',(-0.0721687836487033,0.,0.125));
#16897=CARTESIAN_POINT('',(-0.0627109795608791,0.,0.141381397208144));
#16898=CARTESIAN_POINT('',(-0.0721687836487033,-0.25,0.125));
#16899=CARTESIAN_POINT('',(-0.0721687836487033,0.,0.125));
#16900=CARTESIAN_POINT('',(-0.144337567297406,-0.25,-1.76762539787485E-17));
#16901=CARTESIAN_POINT('Origin',(0.0721687836487032,0.,0.125));
#16902=CARTESIAN_POINT('',(0.0721687836487032,0.,0.125));
#16903=CARTESIAN_POINT('',(0.146084391824352,0.,0.125));
#16904=CARTESIAN_POINT('',(0.0721687836487032,-0.25,0.125));
#16905=CARTESIAN_POINT('',(0.0721687836487032,0.,0.125));
#16906=CARTESIAN_POINT('',(-0.0721687836487033,-0.25,0.125));
#16907=CARTESIAN_POINT('Origin',(0.144337567297406,0.,0.));
#16908=CARTESIAN_POINT('',(0.153795371385231,0.,-0.0163813972081441));
#16909=CARTESIAN_POINT('',(0.0721687836487032,-0.25,0.125));
#16910=CARTESIAN_POINT('Origin',(0.,-0.25,0.));
#16911=CARTESIAN_POINT('Origin',(0.22,0.,0.));
#16912=CARTESIAN_POINT('',(-0.22,-8.67361737988404E-18,-2.69422295812418E-17));
#16913=CARTESIAN_POINT('Origin',(0.,0.,0.));
#16914=CARTESIAN_POINT('Origin',(0.,-0.015,0.));
#16915=CARTESIAN_POINT('',(-0.24505,-0.02505,-3.00099698131059E-17));
#16916=CARTESIAN_POINT('Origin',(0.,-0.02505,0.));
#16917=CARTESIAN_POINT('',(-0.235,-0.015,-2.87791997799628E-17));
#16918=CARTESIAN_POINT('Origin',(0.,-0.3775,0.));
#16919=CARTESIAN_POINT('',(-0.24505,-0.3775,-3.00099698131059E-17));
#16992=UNCERTAINTY_MEASURE_WITH_UNIT(LENGTH_MEASURE(0.001),#17047,
'DISTANCE_ACCURACY_VALUE',
'Maximum model space distance between geometric entities at asserted c
onnectivities');
#16993=UNCERTAINTY_MEASURE_WITH_UNIT(LENGTH_MEASURE(0.001),#17047,
'DISTANCE_ACCURACY_VALUE',
'Maximum model space distance between geometric entities at asserted c
onnectivities');
#17045=(
GEOMETRIC_REPRESENTATION_CONTEXT(3)
GLOBAL_UNCERTAINTY_ASSIGNED_CONTEXT((#16992))
GLOBAL_UNIT_ASSIGNED_CONTEXT((#17047,#17049,#17050))
REPRESENTATION_CONTEXT('','3D')
);
#17046=(
GEOMETRIC_REPRESENTATION_CONTEXT(3)
GLOBAL_UNCERTAINTY_ASSIGNED_CONTEXT((#16993))
GLOBAL_UNIT_ASSIGNED_CONTEXT((#17047,#17049,#17050))
REPRESENTATION_CONTEXT('','3D')
);
#17047=(
LENGTH_UNIT()
NAMED_UNIT(*)
SI_UNIT(.CENTI.,.METRE.)
);
#17049=(
NAMED_UNIT(*)
PLANE_ANGLE_UNIT()
SI_UNIT($,.RADIAN.)
);
#17050=(
NAMED_UNIT(*)
SI_UNIT($,.STERADIAN.)
SOLID_ANGLE_UNIT()
);
#17102=SHAPE_DEFINITION_REPRESENTATION(#17236,#17309);
#17236=PRODUCT_DEFINITION_SHAPE('',$,#17362);
#17309=SHAPE_REPRESENTATION('',(#9737),#17045);
#17310=PRODUCT_DEFINITION_CONTEXT('part definition',#17468,'design');
#17362=PRODUCT_DEFINITION('M5x5 collar screw','M5x5 collar screw',#17414,
#17310);
#17414=PRODUCT_DEFINITION_FORMATION('',$,#17521);
#17468=APPLICATION_CONTEXT(
'Core Data for Automotive Mechanical Design Process');
#17469=PRODUCT_CONTEXT('part definition',#17468,'mechanical');
#17521=PRODUCT('M5x5 collar screw','M5x5 collar screw',
'M5x5 collar screw',(#17469));
#17592=COLOUR_RGB('Black',0.12,0.14,0.17);
#17593=FILL_AREA_STYLE_COLOUR('',#17592);
#17594=FILL_AREA_STYLE('',(#17593));
#17595=SURFACE_STYLE_FILL_AREA(#17594);
#17596=SURFACE_SIDE_STYLE('',(#17595));
#17597=SURFACE_STYLE_USAGE(.BOTH.,#17596);
#17598=PRESENTATION_STYLE_ASSIGNMENT((#17597));
ENDSEC;
END-ISO-10303-21;
